ISO-10303-21;
HEADER;
/* Generated by software containing ST-Developer
 * from STEP Tools, Inc. (www.steptools.com) 
 */

FILE_DESCRIPTION(
/* description */ ('Bin tilter linkage'),
/* implementation_level */ '2;1');

FILE_NAME(
/* name */ 'Screw thrust collar (1).step',
/* time_stamp */ '2026-10-28T03:26:24-07:00',
/* author */ (''),
/* organization */ (''),
/* preprocessor_version */ 'ST-DEVELOPER v20.2',
/* originating_system */ 'Autodesk Translation Framework v15.17.0.0',
/* authorisation */ '');

FILE_SCHEMA (('AUTOMOTIVE_DESIGN { 1 0 10303 214 3 1 1 }'));
ENDSEC;

DATA;
#10=MECHANICAL_DESIGN_GEOMETRIC_PRESENTATION_REPRESENTATION('',(#973),#23728);
#753=SHAPE_REPRESENTATION_RELATIONSHIP('SRR','None',#24225,#859);
#859=ADVANCED_BREP_SHAPE_REPRESENTATION('',(#1084),#23725);
#973=STYLED_ITEM('',(#24772),#1084);
#1084=MANIFOLD_SOLID_BREP('Body1',#12506);
#1488=FACE_BOUND('',#3837,.T.);
#1489=FACE_BOUND('',#3839,.T.);
#1884=PLANE('',#15445);
#1885=PLANE('',#15446);
#2656=FACE_OUTER_BOUND('',#3834,.T.);
#2657=FACE_OUTER_BOUND('',#3835,.T.);
#2658=FACE_OUTER_BOUND('',#3836,.T.);
#2659=FACE_OUTER_BOUND('',#3838,.T.);
#3834=EDGE_LOOP('',(#11237,#11238,#11239,#11240));
#3835=EDGE_LOOP('',(#11241,#11242,#11243,#11244));
#3836=EDGE_LOOP('',(#11245));
#3837=EDGE_LOOP('',(#11246));
#3838=EDGE_LOOP('',(#11247));
#3839=EDGE_LOOP('',(#11248));
#4519=LINE('',#23449,#5194);
#4520=LINE('',#23455,#5195);
#5194=VECTOR('',#19674,0.6);
#5195=VECTOR('',#19681,0.9);
#5947=CIRCLE('',#15440,0.6);
#5948=CIRCLE('',#15441,0.6);
#5949=CIRCLE('',#15443,0.9);
#5950=CIRCLE('',#15444,0.9);
#6916=VERTEX_POINT('',#23446);
#6917=VERTEX_POINT('',#23448);
#6918=VERTEX_POINT('',#23452);
#6919=VERTEX_POINT('',#23454);
#8358=EDGE_CURVE('',#6916,#6916,#5947,.T.);
#8359=EDGE_CURVE('',#6916,#6917,#4519,.T.);
#8360=EDGE_CURVE('',#6917,#6917,#5948,.T.);
#8361=EDGE_CURVE('',#6918,#6918,#5949,.T.);
#8362=EDGE_CURVE('',#6918,#6919,#4520,.T.);
#8363=EDGE_CURVE('',#6919,#6919,#5950,.T.);
#11237=ORIENTED_EDGE('',*,*,#8358,.F.);
#11238=ORIENTED_EDGE('',*,*,#8359,.T.);
#11239=ORIENTED_EDGE('',*,*,#8360,.T.);
#11240=ORIENTED_EDGE('',*,*,#8359,.F.);
#11241=ORIENTED_EDGE('',*,*,#8361,.F.);
#11242=ORIENTED_EDGE('',*,*,#8362,.T.);
#11243=ORIENTED_EDGE('',*,*,#8363,.T.);
#11244=ORIENTED_EDGE('',*,*,#8362,.F.);
#11245=ORIENTED_EDGE('',*,*,#8361,.T.);
#11246=ORIENTED_EDGE('',*,*,#8358,.T.);
#11247=ORIENTED_EDGE('',*,*,#8363,.F.);
#11248=ORIENTED_EDGE('',*,*,#8360,.F.);
#11610=CYLINDRICAL_SURFACE('',#15439,0.6);
#11611=CYLINDRICAL_SURFACE('',#15442,0.9);
#12381=ADVANCED_FACE('',(#2656),#11610,.F.);
#12382=ADVANCED_FACE('',(#2657),#11611,.T.);
#12383=ADVANCED_FACE('',(#2658,#1488),#1884,.T.);
#12384=ADVANCED_FACE('',(#2659,#1489),#1885,.F.);
#12506=CLOSED_SHELL('',(#12381,#12382,#12383,#12384));
#15438=AXIS2_PLACEMENT_3D('',#23444,#19668,#19669);
#15439=AXIS2_PLACEMENT_3D('',#23445,#19670,#19671);
#15440=AXIS2_PLACEMENT_3D('',#23447,#19672,#19673);
#15441=AXIS2_PLACEMENT_3D('',#23450,#19675,#19676);
#15442=AXIS2_PLACEMENT_3D('',#23451,#19677,#19678);
#15443=AXIS2_PLACEMENT_3D('',#23453,#19679,#19680);
#15444=AXIS2_PLACEMENT_3D('',#23456,#19682,#19683);
#15445=AXIS2_PLACEMENT_3D('',#23457,#19684,#19685);
#15446=AXIS2_PLACEMENT_3D('',#23458,#19686,#19687);
#19668=DIRECTION('axis',(0.,0.,1.));
#19669=DIRECTION('refdir',(1.,0.,0.));
#19670=DIRECTION('center_axis',(1.,0.,0.));
#19671=DIRECTION('ref_axis',(0.,0.,-1.));
#19672=DIRECTION('center_axis',(-1.,0.,0.));
#19673=DIRECTION('ref_axis',(0.,0.,-1.));
#19674=DIRECTION('',(-1.,0.,0.));
#19675=DIRECTION('center_axis',(-1.,0.,0.));
#19676=DIRECTION('ref_axis',(0.,0.,-1.));
#19677=DIRECTION('center_axis',(1.,0.,0.));
#19678=DIRECTION('ref_axis',(0.,0.,-1.));
#19679=DIRECTION('center_axis',(1.,0.,0.));
#19680=DIRECTION('ref_axis',(0.,0.,-1.));
#19681=DIRECTION('',(-1.,0.,0.));
#19682=DIRECTION('center_axis',(1.,0.,0.));
#19683=DIRECTION('ref_axis',(0.,0.,-1.));
#19684=DIRECTION('center_axis',(1.,0.,0.));
#19685=DIRECTION('ref_axis',(0.,0.,-1.));
#19686=DIRECTION('center_axis',(1.,0.,0.));
#19687=DIRECTION('ref_axis',(0.,0.,-1.));
#23444=CARTESIAN_POINT('',(0.,0.,0.));
#23445=CARTESIAN_POINT('Origin',(1.,-4.5,8.));
#23446=CARTESIAN_POINT('',(1.2,-4.5,8.6));
#23447=CARTESIAN_POINT('Origin',(1.2,-4.5,8.));
#23448=CARTESIAN_POINT('',(1.,-4.5,8.6));
#23449=CARTESIAN_POINT('',(1.,-4.5,8.6));
#23450=CARTESIAN_POINT('Origin',(1.,-4.5,8.));
#23451=CARTESIAN_POINT('Origin',(1.,-4.5,8.));
#23452=CARTESIAN_POINT('',(1.2,-4.5,8.9));
#23453=CARTESIAN_POINT('Origin',(1.2,-4.5,8.));
#23454=CARTESIAN_POINT('',(1.,-4.5,8.9));
#23455=CARTESIAN_POINT('',(1.,-4.5,8.9));
#23456=CARTESIAN_POINT('Origin',(1.,-4.5,8.));
#23457=CARTESIAN_POINT('Origin',(1.2,-4.5,8.));
#23458=CARTESIAN_POINT('Origin',(1.,-4.5,8.));
#23608=UNCERTAINTY_MEASURE_WITH_UNIT(LENGTH_MEASURE(0.001),#23729,
'DISTANCE_ACCURACY_VALUE',
'Maximum model space distance between geometric entities at asserted c
onnectivities');
#23611=UNCERTAINTY_MEASURE_WITH_UNIT(LENGTH_MEASURE(0.001),#23729,
'DISTANCE_ACCURACY_VALUE',
'Maximum model space distance between geometric entities at asserted c
onnectivities');
#23725=(
GEOMETRIC_REPRESENTATION_CONTEXT(3)
GLOBAL_UNCERTAINTY_ASSIGNED_CONTEXT((#23608))
GLOBAL_UNIT_ASSIGNED_CONTEXT((#23729,#23731,#23732))
REPRESENTATION_CONTEXT('','3D')
);
#23728=(
GEOMETRIC_REPRESENTATION_CONTEXT(3)
GLOBAL_UNCERTAINTY_ASSIGNED_CONTEXT((#23611))
GLOBAL_UNIT_ASSIGNED_CONTEXT((#23729,#23731,#23732))
REPRESENTATION_CONTEXT('','3D')
);
#23729=(
LENGTH_UNIT()
NAMED_UNIT(*)
SI_UNIT(.CENTI.,.METRE.)
);
#23731=(
NAMED_UNIT(*)
PLANE_ANGLE_UNIT()
SI_UNIT($,.RADIAN.)
);
#23732=(
NAMED_UNIT(*)
SI_UNIT($,.STERADIAN.)
SOLID_ANGLE_UNIT()
);
#23846=SHAPE_DEFINITION_REPRESENTATION(#24097,#24225);
#24097=PRODUCT_DEFINITION_SHAPE('',$,#24342);
#24225=SHAPE_REPRESENTATION('',(#15438),#23725);
#24228=PRODUCT_DEFINITION_CONTEXT('part definition',#24578,'design');
#24342=PRODUCT_DEFINITION('Screw thrust collar (1)',
'Screw thrust collar (1)',#24458,#24228);
#24458=PRODUCT_DEFINITION_FORMATION('',$,#24693);
#24578=APPLICATION_CONTEXT(
'Core Data for Automotive Mechanical Design Process');
#24579=PRODUCT_CONTEXT('part definition',#24578,'mechanical');
#24693=PRODUCT('Screw thrust collar (1)','Screw thrust collar (1)',
'Screw thrust collar (1)',(#24579));
#24766=COLOUR_RGB('Black',0.12,0.14,0.17);
#24767=FILL_AREA_STYLE_COLOUR('',#24766);
#24768=FILL_AREA_STYLE('',(#24767));
#24769=SURFACE_STYLE_FILL_AREA(#24768);
#24770=SURFACE_SIDE_STYLE('',(#24769));
#24771=SURFACE_STYLE_USAGE(.BOTH.,#24770);
#24772=PRESENTATION_STYLE_ASSIGNMENT((#24771));
ENDSEC;
END-ISO-10303-21;
